ISO-10303-21;
HEADER;
/* Generated by software containing ST-Developer
 * from STEP Tools, Inc. (www.steptools.com) 
 */

FILE_DESCRIPTION(
/* description */ ('Turntable on roller ring'),
/* implementation_level */ '2;1');

FILE_NAME(
/* name */ 'Table disc.step',
/* time_stamp */ '2026-10-28T03:23:59-07:00',
/* author */ (''),
/* organization */ (''),
/* preprocessor_version */ 'ST-DEVELOPER v20.2',
/* originating_system */ 'Autodesk Translation Framework v15.17.0.0',
/* authorisation */ '');

FILE_SCHEMA (('AUTOMOTIVE_DESIGN { 1 0 10303 214 3 1 1 }'));
ENDSEC;

DATA;
#10=MECHANICAL_DESIGN_GEOMETRIC_PRESENTATION_REPRESENTATION('',(#638),#16281);
#519=SHAPE_REPRESENTATION_RELATIONSHIP('SRR','None',#16535,#574);
#574=ADVANCED_BREP_SHAPE_REPRESENTATION('',(#709),#16229);
#638=STYLED_ITEM('',(#16925),#709);
#709=MANIFOLD_SOLID_BREP('Body1',#8380);
#837=FACE_BOUND('',#2008,.T.);
#838=FACE_BOUND('',#2009,.T.);
#839=FACE_BOUND('',#2010,.T.);
#840=FACE_BOUND('',#2011,.T.);
#841=FACE_BOUND('',#2012,.T.);
#842=FACE_BOUND('',#2013,.T.);
#843=FACE_BOUND('',#2014,.T.);
#844=FACE_BOUND('',#2015,.T.);
#845=FACE_BOUND('',#2016,.T.);
#846=FACE_BOUND('',#2017,.T.);
#847=FACE_BOUND('',#2018,.T.);
#848=FACE_BOUND('',#2019,.T.);
#849=FACE_BOUND('',#2021,.T.);
#850=FACE_BOUND('',#2022,.T.);
#851=FACE_BOUND('',#2023,.T.);
#852=FACE_BOUND('',#2024,.T.);
#853=FACE_BOUND('',#2025,.T.);
#854=FACE_BOUND('',#2026,.T.);
#855=FACE_BOUND('',#2027,.T.);
#856=FACE_BOUND('',#2028,.T.);
#857=FACE_BOUND('',#2029,.T.);
#858=FACE_BOUND('',#2030,.T.);
#859=FACE_BOUND('',#2031,.T.);
#860=FACE_BOUND('',#2032,.T.);
#1057=PLANE('',#9451);
#1058=PLANE('',#9452);
#1409=FACE_OUTER_BOUND('',#1994,.T.);
#1410=FACE_OUTER_BOUND('',#1995,.T.);
#1411=FACE_OUTER_BOUND('',#1996,.T.);
#1412=FACE_OUTER_BOUND('',#1997,.T.);
#1413=FACE_OUTER_BOUND('',#1998,.T.);
#1414=FACE_OUTER_BOUND('',#1999,.T.);
#1415=FACE_OUTER_BOUND('',#2000,.T.);
#1416=FACE_OUTER_BOUND('',#2001,.T.);
#1417=FACE_OUTER_BOUND('',#2002,.T.);
#1418=FACE_OUTER_BOUND('',#2003,.T.);
#1419=FACE_OUTER_BOUND('',#2004,.T.);
#1420=FACE_OUTER_BOUND('',#2005,.T.);
#1421=FACE_OUTER_BOUND('',#2006,.T.);
#1422=FACE_OUTER_BOUND('',#2007,.T.);
#1423=FACE_OUTER_BOUND('',#2020,.T.);
#1994=EDGE_LOOP('',(#6323,#6324,#6325,#6326));
#1995=EDGE_LOOP('',(#6327,#6328,#6329,#6330));
#1996=EDGE_LOOP('',(#6331,#6332,#6333,#6334));
#1997=EDGE_LOOP('',(#6335,#6336,#6337,#6338));
#1998=EDGE_LOOP('',(#6339,#6340,#6341,#6342));
#1999=EDGE_LOOP('',(#6343,#6344,#6345,#6346));
#2000=EDGE_LOOP('',(#6347,#6348,#6349,#6350));
#2001=EDGE_LOOP('',(#6351,#6352,#6353,#6354));
#2002=EDGE_LOOP('',(#6355,#6356,#6357,#6358));
#2003=EDGE_LOOP('',(#6359,#6360,#6361,#6362));
#2004=EDGE_LOOP('',(#6363,#6364,#6365,#6366));
#2005=EDGE_LOOP('',(#6367,#6368,#6369,#6370));
#2006=EDGE_LOOP('',(#6371,#6372,#6373,#6374));
#2007=EDGE_LOOP('',(#6375));
#2008=EDGE_LOOP('',(#6376));
#2009=EDGE_LOOP('',(#6377));
#2010=EDGE_LOOP('',(#6378));
#2011=EDGE_LOOP('',(#6379));
#2012=EDGE_LOOP('',(#6380));
#2013=EDGE_LOOP('',(#6381));
#2014=EDGE_LOOP('',(#6382));
#2015=EDGE_LOOP('',(#6383));
#2016=EDGE_LOOP('',(#6384));
#2017=EDGE_LOOP('',(#6385));
#2018=EDGE_LOOP('',(#6386));
#2019=EDGE_LOOP('',(#6387));
#2020=EDGE_LOOP('',(#6388));
#2021=EDGE_LOOP('',(#6389));
#2022=EDGE_LOOP('',(#6390));
#2023=EDGE_LOOP('',(#6391));
#2024=EDGE_LOOP('',(#6392));
#2025=EDGE_LOOP('',(#6393));
#2026=EDGE_LOOP('',(#6394));
#2027=EDGE_LOOP('',(#6395));
#2028=EDGE_LOOP('',(#6396));
#2029=EDGE_LOOP('',(#6397));
#2030=EDGE_LOOP('',(#6398));
#2031=EDGE_LOOP('',(#6399));
#2032=EDGE_LOOP('',(#6400));
#2623=LINE('',#14135,#3106);
#2624=LINE('',#14141,#3107);
#2625=LINE('',#14147,#3108);
#2626=LINE('',#14153,#3109);
#2627=LINE('',#14159,#3110);
#2628=LINE('',#14165,#3111);
#2629=LINE('',#14171,#3112);
#2630=LINE('',#14177,#3113);
#2631=LINE('',#14183,#3114);
#2632=LINE('',#14189,#3115);
#2633=LINE('',#14195,#3116);
#2634=LINE('',#14201,#3117);
#2635=LINE('',#14207,#3118);
#3106=VECTOR('',#11078,0.225);
#3107=VECTOR('',#11085,0.225);
#3108=VECTOR('',#11092,0.225);
#3109=VECTOR('',#11099,0.25);
#3110=VECTOR('',#11106,0.25);
#3111=VECTOR('',#11113,0.25);
#3112=VECTOR('',#11120,0.25);
#3113=VECTOR('',#11127,0.25);
#3114=VECTOR('',#11134,0.25);
#3115=VECTOR('',#11141,0.25);
#3116=VECTOR('',#11148,0.25);
#3117=VECTOR('',#11155,0.25);
#3118=VECTOR('',#11162,20.);
#3650=CIRCLE('',#9413,0.225);
#3651=CIRCLE('',#9414,0.225);
#3652=CIRCLE('',#9416,0.225);
#3653=CIRCLE('',#9417,0.225);
#3654=CIRCLE('',#9419,0.225);
#3655=CIRCLE('',#9420,0.225);
#3656=CIRCLE('',#9422,0.25);
#3657=CIRCLE('',#9423,0.25);
#3658=CIRCLE('',#9425,0.25);
#3659=CIRCLE('',#9426,0.25);
#3660=CIRCLE('',#9428,0.25);
#3661=CIRCLE('',#9429,0.25);
#3662=CIRCLE('',#9431,0.25);
#3663=CIRCLE('',#9432,0.25);
#3664=CIRCLE('',#9434,0.25);
#3665=CIRCLE('',#9435,0.25);
#3666=CIRCLE('',#9437,0.25);
#3667=CIRCLE('',#9438,0.25);
#3668=CIRCLE('',#9440,0.25);
#3669=CIRCLE('',#9441,0.25);
#3670=CIRCLE('',#9443,0.25);
#3671=CIRCLE('',#9444,0.25);
#3672=CIRCLE('',#9446,0.25);
#3673=CIRCLE('',#9447,0.25);
#3674=CIRCLE('',#9449,20.);
#3675=CIRCLE('',#9450,20.);
#4179=VERTEX_POINT('',#14132);
#4180=VERTEX_POINT('',#14134);
#4181=VERTEX_POINT('',#14138);
#4182=VERTEX_POINT('',#14140);
#4183=VERTEX_POINT('',#14144);
#4184=VERTEX_POINT('',#14146);
#4185=VERTEX_POINT('',#14150);
#4186=VERTEX_POINT('',#14152);
#4187=VERTEX_POINT('',#14156);
#4188=VERTEX_POINT('',#14158);
#4189=VERTEX_POINT('',#14162);
#4190=VERTEX_POINT('',#14164);
#4191=VERTEX_POINT('',#14168);
#4192=VERTEX_POINT('',#14170);
#4193=VERTEX_POINT('',#14174);
#4194=VERTEX_POINT('',#14176);
#4195=VERTEX_POINT('',#14180);
#4196=VERTEX_POINT('',#14182);
#4197=VERTEX_POINT('',#14186);
#4198=VERTEX_POINT('',#14188);
#4199=VERTEX_POINT('',#14192);
#4200=VERTEX_POINT('',#14194);
#4201=VERTEX_POINT('',#14198);
#4202=VERTEX_POINT('',#14200);
#4203=VERTEX_POINT('',#14204);
#4204=VERTEX_POINT('',#14206);
#4972=EDGE_CURVE('',#4179,#4179,#3650,.T.);
#4973=EDGE_CURVE('',#4179,#4180,#2623,.T.);
#4974=EDGE_CURVE('',#4180,#4180,#3651,.T.);
#4975=EDGE_CURVE('',#4181,#4181,#3652,.T.);
#4976=EDGE_CURVE('',#4181,#4182,#2624,.T.);
#4977=EDGE_CURVE('',#4182,#4182,#3653,.T.);
#4978=EDGE_CURVE('',#4183,#4183,#3654,.T.);
#4979=EDGE_CURVE('',#4183,#4184,#2625,.T.);
#4980=EDGE_CURVE('',#4184,#4184,#3655,.T.);
#4981=EDGE_CURVE('',#4185,#4185,#3656,.T.);
#4982=EDGE_CURVE('',#4185,#4186,#2626,.T.);
#4983=EDGE_CURVE('',#4186,#4186,#3657,.T.);
#4984=EDGE_CURVE('',#4187,#4187,#3658,.T.);
#4985=EDGE_CURVE('',#4187,#4188,#2627,.T.);
#4986=EDGE_CURVE('',#4188,#4188,#3659,.T.);
#4987=EDGE_CURVE('',#4189,#4189,#3660,.T.);
#4988=EDGE_CURVE('',#4189,#4190,#2628,.T.);
#4989=EDGE_CURVE('',#4190,#4190,#3661,.T.);
#4990=EDGE_CURVE('',#4191,#4191,#3662,.T.);
#4991=EDGE_CURVE('',#4191,#4192,#2629,.T.);
#4992=EDGE_CURVE('',#4192,#4192,#3663,.T.);
#4993=EDGE_CURVE('',#4193,#4193,#3664,.T.);
#4994=EDGE_CURVE('',#4193,#4194,#2630,.T.);
#4995=EDGE_CURVE('',#4194,#4194,#3665,.T.);
#4996=EDGE_CURVE('',#4195,#4195,#3666,.T.);
#4997=EDGE_CURVE('',#4195,#4196,#2631,.T.);
#4998=EDGE_CURVE('',#4196,#4196,#3667,.T.);
#4999=EDGE_CURVE('',#4197,#4197,#3668,.T.);
#5000=EDGE_CURVE('',#4197,#4198,#2632,.T.);
#5001=EDGE_CURVE('',#4198,#4198,#3669,.T.);
#5002=EDGE_CURVE('',#4199,#4199,#3670,.T.);
#5003=EDGE_CURVE('',#4199,#4200,#2633,.T.);
#5004=EDGE_CURVE('',#4200,#4200,#3671,.T.);
#5005=EDGE_CURVE('',#4201,#4201,#3672,.T.);
#5006=EDGE_CURVE('',#4201,#4202,#2634,.T.);
#5007=EDGE_CURVE('',#4202,#4202,#3673,.T.);
#5008=EDGE_CURVE('',#4203,#4203,#3674,.T.);
#5009=EDGE_CURVE('',#4203,#4204,#2635,.T.);
#5010=EDGE_CURVE('',#4204,#4204,#3675,.T.);
#6323=ORIENTED_EDGE('',*,*,#4972,.F.);
#6324=ORIENTED_EDGE('',*,*,#4973,.T.);
#6325=ORIENTED_EDGE('',*,*,#4974,.F.);
#6326=ORIENTED_EDGE('',*,*,#4973,.F.);
#6327=ORIENTED_EDGE('',*,*,#4975,.F.);
#6328=ORIENTED_EDGE('',*,*,#4976,.T.);
#6329=ORIENTED_EDGE('',*,*,#4977,.F.);
#6330=ORIENTED_EDGE('',*,*,#4976,.F.);
#6331=ORIENTED_EDGE('',*,*,#4978,.F.);
#6332=ORIENTED_EDGE('',*,*,#4979,.T.);
#6333=ORIENTED_EDGE('',*,*,#4980,.F.);
#6334=ORIENTED_EDGE('',*,*,#4979,.F.);
#6335=ORIENTED_EDGE('',*,*,#4981,.F.);
#6336=ORIENTED_EDGE('',*,*,#4982,.T.);
#6337=ORIENTED_EDGE('',*,*,#4983,.F.);
#6338=ORIENTED_EDGE('',*,*,#4982,.F.);
#6339=ORIENTED_EDGE('',*,*,#4984,.F.);
#6340=ORIENTED_EDGE('',*,*,#4985,.T.);
#6341=ORIENTED_EDGE('',*,*,#4986,.F.);
#6342=ORIENTED_EDGE('',*,*,#4985,.F.);
#6343=ORIENTED_EDGE('',*,*,#4987,.F.);
#6344=ORIENTED_EDGE('',*,*,#4988,.T.);
#6345=ORIENTED_EDGE('',*,*,#4989,.F.);
#6346=ORIENTED_EDGE('',*,*,#4988,.F.);
#6347=ORIENTED_EDGE('',*,*,#4990,.F.);
#6348=ORIENTED_EDGE('',*,*,#4991,.T.);
#6349=ORIENTED_EDGE('',*,*,#4992,.F.);
#6350=ORIENTED_EDGE('',*,*,#4991,.F.);
#6351=ORIENTED_EDGE('',*,*,#4993,.F.);
#6352=ORIENTED_EDGE('',*,*,#4994,.T.);
#6353=ORIENTED_EDGE('',*,*,#4995,.F.);
#6354=ORIENTED_EDGE('',*,*,#4994,.F.);
#6355=ORIENTED_EDGE('',*,*,#4996,.F.);
#6356=ORIENTED_EDGE('',*,*,#4997,.T.);
#6357=ORIENTED_EDGE('',*,*,#4998,.F.);
#6358=ORIENTED_EDGE('',*,*,#4997,.F.);
#6359=ORIENTED_EDGE('',*,*,#4999,.F.);
#6360=ORIENTED_EDGE('',*,*,#5000,.T.);
#6361=ORIENTED_EDGE('',*,*,#5001,.F.);
#6362=ORIENTED_EDGE('',*,*,#5000,.F.);
#6363=ORIENTED_EDGE('',*,*,#5002,.F.);
#6364=ORIENTED_EDGE('',*,*,#5003,.T.);
#6365=ORIENTED_EDGE('',*,*,#5004,.F.);
#6366=ORIENTED_EDGE('',*,*,#5003,.F.);
#6367=ORIENTED_EDGE('',*,*,#5005,.F.);
#6368=ORIENTED_EDGE('',*,*,#5006,.T.);
#6369=ORIENTED_EDGE('',*,*,#5007,.F.);
#6370=ORIENTED_EDGE('',*,*,#5006,.F.);
#6371=ORIENTED_EDGE('',*,*,#5008,.F.);
#6372=ORIENTED_EDGE('',*,*,#5009,.T.);
#6373=ORIENTED_EDGE('',*,*,#5010,.T.);
#6374=ORIENTED_EDGE('',*,*,#5009,.F.);
#6375=ORIENTED_EDGE('',*,*,#5008,.T.);
#6376=ORIENTED_EDGE('',*,*,#4983,.T.);
#6377=ORIENTED_EDGE('',*,*,#4986,.T.);
#6378=ORIENTED_EDGE('',*,*,#4989,.T.);
#6379=ORIENTED_EDGE('',*,*,#4992,.T.);
#6380=ORIENTED_EDGE('',*,*,#4995,.T.);
#6381=ORIENTED_EDGE('',*,*,#4998,.T.);
#6382=ORIENTED_EDGE('',*,*,#5001,.T.);
#6383=ORIENTED_EDGE('',*,*,#5004,.T.);
#6384=ORIENTED_EDGE('',*,*,#5007,.T.);
#6385=ORIENTED_EDGE('',*,*,#4980,.T.);
#6386=ORIENTED_EDGE('',*,*,#4977,.T.);
#6387=ORIENTED_EDGE('',*,*,#4974,.T.);
#6388=ORIENTED_EDGE('',*,*,#5010,.F.);
#6389=ORIENTED_EDGE('',*,*,#4981,.T.);
#6390=ORIENTED_EDGE('',*,*,#4984,.T.);
#6391=ORIENTED_EDGE('',*,*,#4987,.T.);
#6392=ORIENTED_EDGE('',*,*,#4990,.T.);
#6393=ORIENTED_EDGE('',*,*,#4993,.T.);
#6394=ORIENTED_EDGE('',*,*,#4996,.T.);
#6395=ORIENTED_EDGE('',*,*,#4999,.T.);
#6396=ORIENTED_EDGE('',*,*,#5002,.T.);
#6397=ORIENTED_EDGE('',*,*,#5005,.T.);
#6398=ORIENTED_EDGE('',*,*,#4978,.T.);
#6399=ORIENTED_EDGE('',*,*,#4975,.T.);
#6400=ORIENTED_EDGE('',*,*,#4972,.T.);
#7734=CYLINDRICAL_SURFACE('',#9412,0.225);
#7735=CYLINDRICAL_SURFACE('',#9415,0.225);
#7736=CYLINDRICAL_SURFACE('',#9418,0.225);
#7737=CYLINDRICAL_SURFACE('',#9421,0.25);
#7738=CYLINDRICAL_SURFACE('',#9424,0.25);
#7739=CYLINDRICAL_SURFACE('',#9427,0.25);
#7740=CYLINDRICAL_SURFACE('',#9430,0.25);
#7741=CYLINDRICAL_SURFACE('',#9433,0.25);
#7742=CYLINDRICAL_SURFACE('',#9436,0.25);
#7743=CYLINDRICAL_SURFACE('',#9439,0.25);
#7744=CYLINDRICAL_SURFACE('',#9442,0.25);
#7745=CYLINDRICAL_SURFACE('',#9445,0.25);
#7746=CYLINDRICAL_SURFACE('',#9448,20.);
#8012=ADVANCED_FACE('',(#1409),#7734,.F.);
#8013=ADVANCED_FACE('',(#1410),#7735,.F.);
#8014=ADVANCED_FACE('',(#1411),#7736,.F.);
#8015=ADVANCED_FACE('',(#1412),#7737,.F.);
#8016=ADVANCED_FACE('',(#1413),#7738,.F.);
#8017=ADVANCED_FACE('',(#1414),#7739,.F.);
#8018=ADVANCED_FACE('',(#1415),#7740,.F.);
#8019=ADVANCED_FACE('',(#1416),#7741,.F.);
#8020=ADVANCED_FACE('',(#1417),#7742,.F.);
#8021=ADVANCED_FACE('',(#1418),#7743,.F.);
#8022=ADVANCED_FACE('',(#1419),#7744,.F.);
#8023=ADVANCED_FACE('',(#1420),#7745,.F.);
#8024=ADVANCED_FACE('',(#1421),#7746,.T.);
#8025=ADVANCED_FACE('',(#1422,#837,#838,#839,#840,#841,#842,#843,#844,#845,
#846,#847,#848),#1057,.T.);
#8026=ADVANCED_FACE('',(#1423,#849,#850,#851,#852,#853,#854,#855,#856,#857,
#858,#859,#860),#1058,.F.);
#8380=CLOSED_SHELL('',(#8012,#8013,#8014,#8015,#8016,#8017,#8018,#8019,
#8020,#8021,#8022,#8023,#8024,#8025,#8026));
#9411=AXIS2_PLACEMENT_3D('',#14130,#11072,#11073);
#9412=AXIS2_PLACEMENT_3D('',#14131,#11074,#11075);
#9413=AXIS2_PLACEMENT_3D('',#14133,#11076,#11077);
#9414=AXIS2_PLACEMENT_3D('',#14136,#11079,#11080);
#9415=AXIS2_PLACEMENT_3D('',#14137,#11081,#11082);
#9416=AXIS2_PLACEMENT_3D('',#14139,#11083,#11084);
#9417=AXIS2_PLACEMENT_3D('',#14142,#11086,#11087);
#9418=AXIS2_PLACEMENT_3D('',#14143,#11088,#11089);
#9419=AXIS2_PLACEMENT_3D('',#14145,#11090,#11091);
#9420=AXIS2_PLACEMENT_3D('',#14148,#11093,#11094);
#9421=AXIS2_PLACEMENT_3D('',#14149,#11095,#11096);
#9422=AXIS2_PLACEMENT_3D('',#14151,#11097,#11098);
#9423=AXIS2_PLACEMENT_3D('',#14154,#11100,#11101);
#9424=AXIS2_PLACEMENT_3D('',#14155,#11102,#11103);
#9425=AXIS2_PLACEMENT_3D('',#14157,#11104,#11105);
#9426=AXIS2_PLACEMENT_3D('',#14160,#11107,#11108);
#9427=AXIS2_PLACEMENT_3D('',#14161,#11109,#11110);
#9428=AXIS2_PLACEMENT_3D('',#14163,#11111,#11112);
#9429=AXIS2_PLACEMENT_3D('',#14166,#11114,#11115);
#9430=AXIS2_PLACEMENT_3D('',#14167,#11116,#11117);
#9431=AXIS2_PLACEMENT_3D('',#14169,#11118,#11119);
#9432=AXIS2_PLACEMENT_3D('',#14172,#11121,#11122);
#9433=AXIS2_PLACEMENT_3D('',#14173,#11123,#11124);
#9434=AXIS2_PLACEMENT_3D('',#14175,#11125,#11126);
#9435=AXIS2_PLACEMENT_3D('',#14178,#11128,#11129);
#9436=AXIS2_PLACEMENT_3D('',#14179,#11130,#11131);
#9437=AXIS2_PLACEMENT_3D('',#14181,#11132,#11133);
#9438=AXIS2_PLACEMENT_3D('',#14184,#11135,#11136);
#9439=AXIS2_PLACEMENT_3D('',#14185,#11137,#11138);
#9440=AXIS2_PLACEMENT_3D('',#14187,#11139,#11140);
#9441=AXIS2_PLACEMENT_3D('',#14190,#11142,#11143);
#9442=AXIS2_PLACEMENT_3D('',#14191,#11144,#11145);
#9443=AXIS2_PLACEMENT_3D('',#14193,#11146,#11147);
#9444=AXIS2_PLACEMENT_3D('',#14196,#11149,#11150);
#9445=AXIS2_PLACEMENT_3D('',#14197,#11151,#11152);
#9446=AXIS2_PLACEMENT_3D('',#14199,#11153,#11154);
#9447=AXIS2_PLACEMENT_3D('',#14202,#11156,#11157);
#9448=AXIS2_PLACEMENT_3D('',#14203,#11158,#11159);
#9449=AXIS2_PLACEMENT_3D('',#14205,#11160,#11161);
#9450=AXIS2_PLACEMENT_3D('',#14208,#11163,#11164);
#9451=AXIS2_PLACEMENT_3D('',#14209,#11165,#11166);
#9452=AXIS2_PLACEMENT_3D('',#14210,#11167,#11168);
#11072=DIRECTION('axis',(0.,0.,1.));
#11073=DIRECTION('refdir',(1.,0.,0.));
#11074=DIRECTION('center_axis',(0.,0.,1.));
#11075=DIRECTION('ref_axis',(1.,0.,0.));
#11076=DIRECTION('center_axis',(0.,0.,1.));
#11077=DIRECTION('ref_axis',(1.,0.,0.));
#11078=DIRECTION('',(0.,0.,1.));
#11079=DIRECTION('center_axis',(0.,0.,-1.));
#11080=DIRECTION('ref_axis',(1.,0.,0.));
#11081=DIRECTION('center_axis',(0.,0.,1.));
#11082=DIRECTION('ref_axis',(1.,0.,0.));
#11083=DIRECTION('center_axis',(0.,0.,1.));
#11084=DIRECTION('ref_axis',(1.,0.,0.));
#11085=DIRECTION('',(0.,0.,1.));
#11086=DIRECTION('center_axis',(0.,0.,-1.));
#11087=DIRECTION('ref_axis',(1.,0.,0.));
#11088=DIRECTION('center_axis',(0.,0.,1.));
#11089=DIRECTION('ref_axis',(1.,0.,0.));
#11090=DIRECTION('center_axis',(0.,0.,1.));
#11091=DIRECTION('ref_axis',(1.,0.,0.));
#11092=DIRECTION('',(0.,0.,1.));
#11093=DIRECTION('center_axis',(0.,0.,-1.));
#11094=DIRECTION('ref_axis',(1.,0.,0.));
#11095=DIRECTION('center_axis',(0.,0.,1.));
#11096=DIRECTION('ref_axis',(1.,0.,0.));
#11097=DIRECTION('center_axis',(0.,0.,1.));
#11098=DIRECTION('ref_axis',(1.,0.,0.));
#11099=DIRECTION('',(0.,0.,1.));
#11100=DIRECTION('center_axis',(0.,0.,-1.));
#11101=DIRECTION('ref_axis',(1.,0.,0.));
#11102=DIRECTION('center_axis',(0.,0.,1.));
#11103=DIRECTION('ref_axis',(1.,0.,0.));
#11104=DIRECTION('center_axis',(0.,0.,1.));
#11105=DIRECTION('ref_axis',(1.,0.,0.));
#11106=DIRECTION('',(0.,0.,1.));
#11107=DIRECTION('center_axis',(0.,0.,-1.));
#11108=DIRECTION('ref_axis',(1.,0.,0.));
#11109=DIRECTION('center_axis',(0.,0.,1.));
#11110=DIRECTION('ref_axis',(1.,0.,0.));
#11111=DIRECTION('center_axis',(0.,0.,1.));
#11112=DIRECTION('ref_axis',(1.,0.,0.));
#11113=DIRECTION('',(0.,0.,1.));
#11114=DIRECTION('center_axis',(0.,0.,-1.));
#11115=DIRECTION('ref_axis',(1.,0.,0.));
#11116=DIRECTION('center_axis',(0.,0.,1.));
#11117=DIRECTION('ref_axis',(1.,0.,0.));
#11118=DIRECTION('center_axis',(0.,0.,1.));
#11119=DIRECTION('ref_axis',(1.,0.,0.));
#11120=DIRECTION('',(0.,0.,1.));
#11121=DIRECTION('center_axis',(0.,0.,-1.));
#11122=DIRECTION('ref_axis',(1.,0.,0.));
#11123=DIRECTION('center_axis',(0.,0.,1.));
#11124=DIRECTION('ref_axis',(1.,0.,0.));
#11125=DIRECTION('center_axis',(0.,0.,1.));
#11126=DIRECTION('ref_axis',(1.,0.,0.));
#11127=DIRECTION('',(0.,0.,1.));
#11128=DIRECTION('center_axis',(0.,0.,-1.));
#11129=DIRECTION('ref_axis',(1.,0.,0.));
#11130=DIRECTION('center_axis',(0.,0.,1.));
#11131=DIRECTION('ref_axis',(1.,0.,0.));
#11132=DIRECTION('center_axis',(0.,0.,1.));
#11133=DIRECTION('ref_axis',(1.,0.,0.));
#11134=DIRECTION('',(0.,0.,1.));
#11135=DIRECTION('center_axis',(0.,0.,-1.));
#11136=DIRECTION('ref_axis',(1.,0.,0.));
#11137=DIRECTION('center_axis',(0.,0.,1.));
#11138=DIRECTION('ref_axis',(1.,0.,0.));
#11139=DIRECTION('center_axis',(0.,0.,1.));
#11140=DIRECTION('ref_axis',(1.,0.,0.));
#11141=DIRECTION('',(0.,0.,1.));
#11142=DIRECTION('center_axis',(0.,0.,-1.));
#11143=DIRECTION('ref_axis',(1.,0.,0.));
#11144=DIRECTION('center_axis',(0.,0.,1.));
#11145=DIRECTION('ref_axis',(1.,0.,0.));
#11146=DIRECTION('center_axis',(0.,0.,1.));
#11147=DIRECTION('ref_axis',(1.,0.,0.));
#11148=DIRECTION('',(0.,0.,1.));
#11149=DIRECTION('center_axis',(0.,0.,-1.));
#11150=DIRECTION('ref_axis',(1.,0.,0.));
#11151=DIRECTION('center_axis',(0.,0.,1.));
#11152=DIRECTION('ref_axis',(1.,0.,0.));
#11153=DIRECTION('center_axis',(0.,0.,1.));
#11154=DIRECTION('ref_axis',(1.,0.,0.));
#11155=DIRECTION('',(0.,0.,1.));
#11156=DIRECTION('center_axis',(0.,0.,-1.));
#11157=DIRECTION('ref_axis',(1.,0.,0.));
#11158=DIRECTION('center_axis',(0.,0.,1.));
#11159=DIRECTION('ref_axis',(1.,0.,0.));
#11160=DIRECTION('center_axis',(0.,0.,1.));
#11161=DIRECTION('ref_axis',(1.,0.,0.));
#11162=DIRECTION('',(0.,0.,-1.));
#11163=DIRECTION('center_axis',(0.,0.,1.));
#11164=DIRECTION('ref_axis',(1.,0.,0.));
#11165=DIRECTION('center_axis',(0.,0.,1.));
#11166=DIRECTION('ref_axis',(1.,0.,0.));
#11167=DIRECTION('center_axis',(0.,0.,1.));
#11168=DIRECTION('ref_axis',(1.,0.,0.));
#14130=CARTESIAN_POINT('',(0.,0.,0.));
#14131=CARTESIAN_POINT('Origin',(1.2,0.,5.4));
#14132=CARTESIAN_POINT('',(0.975,-2.75545529808155E-17,5.5));
#14133=CARTESIAN_POINT('Origin',(1.2,0.,5.5));
#14134=CARTESIAN_POINT('',(0.975,2.75545529808155E-17,6.7));
#14135=CARTESIAN_POINT('',(0.975,-2.75545529808155E-17,5.4));
#14136=CARTESIAN_POINT('Origin',(1.2,0.,6.7));
#14137=CARTESIAN_POINT('Origin',(-0.6,1.03923048454133,5.4));
#14138=CARTESIAN_POINT('',(-0.825,1.03923048454133,5.5));
#14139=CARTESIAN_POINT('Origin',(-0.6,1.03923048454133,5.5));
#14140=CARTESIAN_POINT('',(-0.825,1.03923048454133,6.7));
#14141=CARTESIAN_POINT('',(-0.825,1.03923048454133,5.4));
#14142=CARTESIAN_POINT('Origin',(-0.6,1.03923048454133,6.7));
#14143=CARTESIAN_POINT('Origin',(-0.600000000000001,-1.03923048454133,5.4));
#14144=CARTESIAN_POINT('',(-0.825000000000001,-1.03923048454133,5.5));
#14145=CARTESIAN_POINT('Origin',(-0.600000000000001,-1.03923048454133,5.5));
#14146=CARTESIAN_POINT('',(-0.825000000000001,-1.03923048454133,6.7));
#14147=CARTESIAN_POINT('',(-0.825000000000001,-1.03923048454133,5.4));
#14148=CARTESIAN_POINT('Origin',(-0.600000000000001,-1.03923048454133,6.7));
#14149=CARTESIAN_POINT('Origin',(7.,0.,5.4));
#14150=CARTESIAN_POINT('',(6.75,-3.06161699786838E-17,5.5));
#14151=CARTESIAN_POINT('Origin',(7.,0.,5.5));
#14152=CARTESIAN_POINT('',(6.75,3.06161699786838E-17,6.7));
#14153=CARTESIAN_POINT('',(6.75,-3.06161699786838E-17,5.4));
#14154=CARTESIAN_POINT('Origin',(7.,0.,6.7));
#14155=CARTESIAN_POINT('Origin',(0.,7.,5.4));
#14156=CARTESIAN_POINT('',(-0.25,7.,5.5));
#14157=CARTESIAN_POINT('Origin',(0.,7.,5.5));
#14158=CARTESIAN_POINT('',(-0.25,7.,6.7));
#14159=CARTESIAN_POINT('',(-0.25,7.,5.4));
#14160=CARTESIAN_POINT('Origin',(0.,7.,6.7));
#14161=CARTESIAN_POINT('Origin',(0.,0.,5.4));
#14162=CARTESIAN_POINT('',(-0.25,-3.06161699786838E-17,5.5));
#14163=CARTESIAN_POINT('Origin',(0.,0.,5.5));
#14164=CARTESIAN_POINT('',(-0.25,3.06161699786838E-17,6.7));
#14165=CARTESIAN_POINT('',(-0.25,-3.06161699786838E-17,5.4));
#14166=CARTESIAN_POINT('Origin',(0.,0.,6.7));
#14167=CARTESIAN_POINT('Origin',(-7.,7.,5.4));
#14168=CARTESIAN_POINT('',(-7.25,7.,5.5));
#14169=CARTESIAN_POINT('Origin',(-7.,7.,5.5));
#14170=CARTESIAN_POINT('',(-7.25,7.,6.7));
#14171=CARTESIAN_POINT('',(-7.25,7.,5.4));
#14172=CARTESIAN_POINT('Origin',(-7.,7.,6.7));
#14173=CARTESIAN_POINT('Origin',(-7.,0.,5.4));
#14174=CARTESIAN_POINT('',(-7.25,-3.06161699786838E-17,5.5));
#14175=CARTESIAN_POINT('Origin',(-7.,0.,5.5));
#14176=CARTESIAN_POINT('',(-7.25,3.06161699786838E-17,6.7));
#14177=CARTESIAN_POINT('',(-7.25,-3.06161699786838E-17,5.4));
#14178=CARTESIAN_POINT('Origin',(-7.,0.,6.7));
#14179=CARTESIAN_POINT('Origin',(0.,-7.,5.4));
#14180=CARTESIAN_POINT('',(-0.25,-7.,5.5));
#14181=CARTESIAN_POINT('Origin',(0.,-7.,5.5));
#14182=CARTESIAN_POINT('',(-0.25,-7.,6.7));
#14183=CARTESIAN_POINT('',(-0.25,-7.,5.4));
#14184=CARTESIAN_POINT('Origin',(0.,-7.,6.7));
#14185=CARTESIAN_POINT('Origin',(-7.,-7.,5.4));
#14186=CARTESIAN_POINT('',(-7.25,-7.,5.5));
#14187=CARTESIAN_POINT('Origin',(-7.,-7.,5.5));
#14188=CARTESIAN_POINT('',(-7.25,-7.,6.7));
#14189=CARTESIAN_POINT('',(-7.25,-7.,5.4));
#14190=CARTESIAN_POINT('Origin',(-7.,-7.,6.7));
#14191=CARTESIAN_POINT('Origin',(7.,-7.,5.4));
#14192=CARTESIAN_POINT('',(6.75,-7.,5.5));
#14193=CARTESIAN_POINT('Origin',(7.,-7.,5.5));
#14194=CARTESIAN_POINT('',(6.75,-7.,6.7));
#14195=CARTESIAN_POINT('',(6.75,-7.,5.4));
#14196=CARTESIAN_POINT('Origin',(7.,-7.,6.7));
#14197=CARTESIAN_POINT('Origin',(7.,7.,5.4));
#14198=CARTESIAN_POINT('',(6.75,7.,5.5));
#14199=CARTESIAN_POINT('Origin',(7.,7.,5.5));
#14200=CARTESIAN_POINT('',(6.75,7.,6.7));
#14201=CARTESIAN_POINT('',(6.75,7.,5.4));
#14202=CARTESIAN_POINT('Origin',(7.,7.,6.7));
#14203=CARTESIAN_POINT('Origin',(0.,0.,5.5));
#14204=CARTESIAN_POINT('',(-20.,-2.44929359829471E-15,6.7));
#14205=CARTESIAN_POINT('Origin',(0.,0.,6.7));
#14206=CARTESIAN_POINT('',(-20.,-2.44929359829471E-15,5.5));
#14207=CARTESIAN_POINT('',(-20.,-2.44929359829471E-15,5.5));
#14208=CARTESIAN_POINT('Origin',(0.,0.,5.5));
#14209=CARTESIAN_POINT('Origin',(0.,0.,6.7));
#14210=CARTESIAN_POINT('Origin',(0.,0.,5.5));
#16160=UNCERTAINTY_MEASURE_WITH_UNIT(LENGTH_MEASURE(0.001),#16282,
'DISTANCE_ACCURACY_VALUE',
'Maximum model space distance between geometric entities at asserted c
onnectivities');
#16212=UNCERTAINTY_MEASURE_WITH_UNIT(LENGTH_MEASURE(0.001),#16282,
'DISTANCE_ACCURACY_VALUE',
'Maximum model space distance between geometric entities at asserted c
onnectivities');
#16229=(
GEOMETRIC_REPRESENTATION_CONTEXT(3)
GLOBAL_UNCERTAINTY_ASSIGNED_CONTEXT((#16160))
GLOBAL_UNIT_ASSIGNED_CONTEXT((#16282,#16284,#16285))
REPRESENTATION_CONTEXT('','3D')
);
#16281=(
GEOMETRIC_REPRESENTATION_CONTEXT(3)
GLOBAL_UNCERTAINTY_ASSIGNED_CONTEXT((#16212))
GLOBAL_UNIT_ASSIGNED_CONTEXT((#16282,#16284,#16285))
REPRESENTATION_CONTEXT('','3D')
);
#16282=(
LENGTH_UNIT()
NAMED_UNIT(*)
SI_UNIT(.CENTI.,.METRE.)
);
#16284=(
NAMED_UNIT(*)
PLANE_ANGLE_UNIT()
SI_UNIT($,.RADIAN.)
);
#16285=(
NAMED_UNIT(*)
SI_UNIT($,.STERADIAN.)
SOLID_ANGLE_UNIT()
);
#16302=SHAPE_DEFINITION_REPRESENTATION(#16375,#16535);
#16375=PRODUCT_DEFINITION_SHAPE('',$,#16604);
#16535=SHAPE_REPRESENTATION('',(#9411),#16229);
#16587=PRODUCT_DEFINITION_CONTEXT('part definition',#16793,'design');
#16604=PRODUCT_DEFINITION('Table disc','Table disc',#16672,#16587);
#16672=PRODUCT_DEFINITION_FORMATION('',$,#16811);
#16793=APPLICATION_CONTEXT(
'Core Data for Automotive Mechanical Design Process');
#16794=PRODUCT_CONTEXT('part definition',#16793,'mechanical');
#16811=PRODUCT('Table disc','Table disc','Table disc',(#16794));
#16919=COLOUR_RGB('Sky Blue',0.24,0.69,0.87);
#16920=FILL_AREA_STYLE_COLOUR('',#16919);
#16921=FILL_AREA_STYLE('',(#16920));
#16922=SURFACE_STYLE_FILL_AREA(#16921);
#16923=SURFACE_SIDE_STYLE('',(#16922));
#16924=SURFACE_STYLE_USAGE(.BOTH.,#16923);
#16925=PRESENTATION_STYLE_ASSIGNMENT((#16924));
ENDSEC;
END-ISO-10303-21;
